ISO-10303-21;
HEADER;
/* Generated by software containing ST-Developer
 * from STEP Tools, Inc. (www.steptools.com) 
 */

FILE_DESCRIPTION(
/* description */ ('Four-bar parallelogram arm'),
/* implementation_level */ '2;1');

FILE_NAME(
/* name */ 'Bearing cap (4).step',
/* time_stamp */ '2026-10-28T03:24:55-07:00',
/* author */ (''),
/* organization */ (''),
/* preprocessor_version */ 'ST-DEVELOPER v20.2',
/* originating_system */ 'Autodesk Translation Framework v15.17.0.0',
/* authorisation */ '');

FILE_SCHEMA (('AUTOMOTIVE_DESIGN { 1 0 10303 214 3 1 1 }'));
ENDSEC;

DATA;
#10=MECHANICAL_DESIGN_GEOMETRIC_PRESENTATION_REPRESENTATION('',(#649),#14512);
#549=SHAPE_REPRESENTATION_RELATIONSHIP('SRR','None',#14772,#599);
#599=ADVANCED_BREP_SHAPE_REPRESENTATION('',(#706),#14487);
#649=STYLED_ITEM('',(#15087),#706);
#706=MANIFOLD_SOLID_BREP('Body1',#7354);
#895=FACE_BOUND('',#2011,.T.);
#896=FACE_BOUND('',#2012,.T.);
#897=FACE_BOUND('',#2013,.T.);
#898=FACE_BOUND('',#2014,.T.);
#899=FACE_BOUND('',#2015,.T.);
#900=FACE_BOUND('',#2017,.T.);
#901=FACE_BOUND('',#2018,.T.);
#902=FACE_BOUND('',#2019,.T.);
#903=FACE_BOUND('',#2020,.T.);
#904=FACE_BOUND('',#2021,.T.);
#1117=PLANE('',#8432);
#1118=PLANE('',#8433);
#1424=FACE_OUTER_BOUND('',#2004,.T.);
#1425=FACE_OUTER_BOUND('',#2005,.T.);
#1426=FACE_OUTER_BOUND('',#2006,.T.);
#1427=FACE_OUTER_BOUND('',#2007,.T.);
#1428=FACE_OUTER_BOUND('',#2008,.T.);
#1429=FACE_OUTER_BOUND('',#2009,.T.);
#1430=FACE_OUTER_BOUND('',#2010,.T.);
#1431=FACE_OUTER_BOUND('',#2016,.T.);
#2004=EDGE_LOOP('',(#5928,#5929,#5930,#5931));
#2005=EDGE_LOOP('',(#5932,#5933,#5934,#5935));
#2006=EDGE_LOOP('',(#5936,#5937,#5938,#5939));
#2007=EDGE_LOOP('',(#5940,#5941,#5942,#5943));
#2008=EDGE_LOOP('',(#5944,#5945,#5946,#5947));
#2009=EDGE_LOOP('',(#5948,#5949,#5950,#5951));
#2010=EDGE_LOOP('',(#5952));
#2011=EDGE_LOOP('',(#5953));
#2012=EDGE_LOOP('',(#5954));
#2013=EDGE_LOOP('',(#5955));
#2014=EDGE_LOOP('',(#5956));
#2015=EDGE_LOOP('',(#5957));
#2016=EDGE_LOOP('',(#5958));
#2017=EDGE_LOOP('',(#5959));
#2018=EDGE_LOOP('',(#5960));
#2019=EDGE_LOOP('',(#5961));
#2020=EDGE_LOOP('',(#5962));
#2021=EDGE_LOOP('',(#5963));
#2554=LINE('',#13070,#2948);
#2555=LINE('',#13076,#2949);
#2556=LINE('',#13082,#2950);
#2557=LINE('',#13088,#2951);
#2558=LINE('',#13094,#2952);
#2559=LINE('',#13100,#2953);
#2948=VECTOR('',#10168,0.225);
#2949=VECTOR('',#10175,0.225);
#2950=VECTOR('',#10182,0.225);
#2951=VECTOR('',#10189,0.225);
#2952=VECTOR('',#10196,1.02);
#2953=VECTOR('',#10203,2.2);
#3322=CIRCLE('',#8415,0.225);
#3323=CIRCLE('',#8416,0.225);
#3324=CIRCLE('',#8418,0.225);
#3325=CIRCLE('',#8419,0.225);
#3326=CIRCLE('',#8421,0.225);
#3327=CIRCLE('',#8422,0.225);
#3328=CIRCLE('',#8424,0.225);
#3329=CIRCLE('',#8425,0.225);
#3330=CIRCLE('',#8427,1.02);
#3331=CIRCLE('',#8428,1.02);
#3332=CIRCLE('',#8430,2.2);
#3333=CIRCLE('',#8431,2.2);
#3856=VERTEX_POINT('',#13067);
#3857=VERTEX_POINT('',#13069);
#3858=VERTEX_POINT('',#13073);
#3859=VERTEX_POINT('',#13075);
#3860=VERTEX_POINT('',#13079);
#3861=VERTEX_POINT('',#13081);
#3862=VERTEX_POINT('',#13085);
#3863=VERTEX_POINT('',#13087);
#3864=VERTEX_POINT('',#13091);
#3865=VERTEX_POINT('',#13093);
#3866=VERTEX_POINT('',#13097);
#3867=VERTEX_POINT('',#13099);
#4595=EDGE_CURVE('',#3856,#3856,#3322,.T.);
#4596=EDGE_CURVE('',#3856,#3857,#2554,.T.);
#4597=EDGE_CURVE('',#3857,#3857,#3323,.T.);
#4598=EDGE_CURVE('',#3858,#3858,#3324,.T.);
#4599=EDGE_CURVE('',#3858,#3859,#2555,.T.);
#4600=EDGE_CURVE('',#3859,#3859,#3325,.T.);
#4601=EDGE_CURVE('',#3860,#3860,#3326,.T.);
#4602=EDGE_CURVE('',#3860,#3861,#2556,.T.);
#4603=EDGE_CURVE('',#3861,#3861,#3327,.T.);
#4604=EDGE_CURVE('',#3862,#3862,#3328,.T.);
#4605=EDGE_CURVE('',#3862,#3863,#2557,.T.);
#4606=EDGE_CURVE('',#3863,#3863,#3329,.T.);
#4607=EDGE_CURVE('',#3864,#3864,#3330,.T.);
#4608=EDGE_CURVE('',#3864,#3865,#2558,.T.);
#4609=EDGE_CURVE('',#3865,#3865,#3331,.T.);
#4610=EDGE_CURVE('',#3866,#3866,#3332,.T.);
#4611=EDGE_CURVE('',#3866,#3867,#2559,.T.);
#4612=EDGE_CURVE('',#3867,#3867,#3333,.T.);
#5928=ORIENTED_EDGE('',*,*,#4595,.F.);
#5929=ORIENTED_EDGE('',*,*,#4596,.T.);
#5930=ORIENTED_EDGE('',*,*,#4597,.F.);
#5931=ORIENTED_EDGE('',*,*,#4596,.F.);
#5932=ORIENTED_EDGE('',*,*,#4598,.F.);
#5933=ORIENTED_EDGE('',*,*,#4599,.T.);
#5934=ORIENTED_EDGE('',*,*,#4600,.F.);
#5935=ORIENTED_EDGE('',*,*,#4599,.F.);
#5936=ORIENTED_EDGE('',*,*,#4601,.F.);
#5937=ORIENTED_EDGE('',*,*,#4602,.T.);
#5938=ORIENTED_EDGE('',*,*,#4603,.F.);
#5939=ORIENTED_EDGE('',*,*,#4602,.F.);
#5940=ORIENTED_EDGE('',*,*,#4604,.F.);
#5941=ORIENTED_EDGE('',*,*,#4605,.T.);
#5942=ORIENTED_EDGE('',*,*,#4606,.F.);
#5943=ORIENTED_EDGE('',*,*,#4605,.F.);
#5944=ORIENTED_EDGE('',*,*,#4607,.F.);
#5945=ORIENTED_EDGE('',*,*,#4608,.T.);
#5946=ORIENTED_EDGE('',*,*,#4609,.T.);
#5947=ORIENTED_EDGE('',*,*,#4608,.F.);
#5948=ORIENTED_EDGE('',*,*,#4610,.F.);
#5949=ORIENTED_EDGE('',*,*,#4611,.T.);
#5950=ORIENTED_EDGE('',*,*,#4612,.T.);
#5951=ORIENTED_EDGE('',*,*,#4611,.F.);
#5952=ORIENTED_EDGE('',*,*,#4610,.T.);
#5953=ORIENTED_EDGE('',*,*,#4607,.T.);
#5954=ORIENTED_EDGE('',*,*,#4606,.T.);
#5955=ORIENTED_EDGE('',*,*,#4603,.T.);
#5956=ORIENTED_EDGE('',*,*,#4600,.T.);
#5957=ORIENTED_EDGE('',*,*,#4597,.T.);
#5958=ORIENTED_EDGE('',*,*,#4612,.F.);
#5959=ORIENTED_EDGE('',*,*,#4609,.F.);
#5960=ORIENTED_EDGE('',*,*,#4604,.T.);
#5961=ORIENTED_EDGE('',*,*,#4601,.T.);
#5962=ORIENTED_EDGE('',*,*,#4598,.T.);
#5963=ORIENTED_EDGE('',*,*,#4595,.T.);
#6822=CYLINDRICAL_SURFACE('',#8414,0.225);
#6823=CYLINDRICAL_SURFACE('',#8417,0.225);
#6824=CYLINDRICAL_SURFACE('',#8420,0.225);
#6825=CYLINDRICAL_SURFACE('',#8423,0.225);
#6826=CYLINDRICAL_SURFACE('',#8426,1.02);
#6827=CYLINDRICAL_SURFACE('',#8429,2.2);
#7129=ADVANCED_FACE('',(#1424),#6822,.F.);
#7130=ADVANCED_FACE('',(#1425),#6823,.F.);
#7131=ADVANCED_FACE('',(#1426),#6824,.F.);
#7132=ADVANCED_FACE('',(#1427),#6825,.F.);
#7133=ADVANCED_FACE('',(#1428),#6826,.F.);
#7134=ADVANCED_FACE('',(#1429),#6827,.T.);
#7135=ADVANCED_FACE('',(#1430,#895,#896,#897,#898,#899),#1117,.T.);
#7136=ADVANCED_FACE('',(#1431,#900,#901,#902,#903,#904),#1118,.F.);
#7354=CLOSED_SHELL('',(#7129,#7130,#7131,#7132,#7133,#7134,#7135,#7136));
#8413=AXIS2_PLACEMENT_3D('',#13065,#10162,#10163);
#8414=AXIS2_PLACEMENT_3D('',#13066,#10164,#10165);
#8415=AXIS2_PLACEMENT_3D('',#13068,#10166,#10167);
#8416=AXIS2_PLACEMENT_3D('',#13071,#10169,#10170);
#8417=AXIS2_PLACEMENT_3D('',#13072,#10171,#10172);
#8418=AXIS2_PLACEMENT_3D('',#13074,#10173,#10174);
#8419=AXIS2_PLACEMENT_3D('',#13077,#10176,#10177);
#8420=AXIS2_PLACEMENT_3D('',#13078,#10178,#10179);
#8421=AXIS2_PLACEMENT_3D('',#13080,#10180,#10181);
#8422=AXIS2_PLACEMENT_3D('',#13083,#10183,#10184);
#8423=AXIS2_PLACEMENT_3D('',#13084,#10185,#10186);
#8424=AXIS2_PLACEMENT_3D('',#13086,#10187,#10188);
#8425=AXIS2_PLACEMENT_3D('',#13089,#10190,#10191);
#8426=AXIS2_PLACEMENT_3D('',#13090,#10192,#10193);
#8427=AXIS2_PLACEMENT_3D('',#13092,#10194,#10195);
#8428=AXIS2_PLACEMENT_3D('',#13095,#10197,#10198);
#8429=AXIS2_PLACEMENT_3D('',#13096,#10199,#10200);
#8430=AXIS2_PLACEMENT_3D('',#13098,#10201,#10202);
#8431=AXIS2_PLACEMENT_3D('',#13101,#10204,#10205);
#8432=AXIS2_PLACEMENT_3D('',#13102,#10206,#10207);
#8433=AXIS2_PLACEMENT_3D('',#13103,#10208,#10209);
#10162=DIRECTION('axis',(0.,0.,1.));
#10163=DIRECTION('refdir',(1.,0.,0.));
#10164=DIRECTION('center_axis',(0.,1.,0.));
#10165=DIRECTION('ref_axis',(1.,0.,0.));
#10166=DIRECTION('center_axis',(0.,1.,0.));
#10167=DIRECTION('ref_axis',(1.,0.,0.));
#10168=DIRECTION('',(0.,1.,0.));
#10169=DIRECTION('center_axis',(0.,-1.,0.));
#10170=DIRECTION('ref_axis',(1.,0.,0.));
#10171=DIRECTION('center_axis',(0.,1.,0.));
#10172=DIRECTION('ref_axis',(1.,0.,0.));
#10173=DIRECTION('center_axis',(0.,1.,0.));
#10174=DIRECTION('ref_axis',(1.,0.,0.));
#10175=DIRECTION('',(0.,1.,0.));
#10176=DIRECTION('center_axis',(0.,-1.,0.));
#10177=DIRECTION('ref_axis',(1.,0.,0.));
#10178=DIRECTION('center_axis',(0.,1.,0.));
#10179=DIRECTION('ref_axis',(1.,0.,0.));
#10180=DIRECTION('center_axis',(0.,1.,0.));
#10181=DIRECTION('ref_axis',(1.,0.,0.));
#10182=DIRECTION('',(0.,1.,0.));
#10183=DIRECTION('center_axis',(0.,-1.,0.));
#10184=DIRECTION('ref_axis',(1.,0.,0.));
#10185=DIRECTION('center_axis',(0.,1.,0.));
#10186=DIRECTION('ref_axis',(1.,0.,0.));
#10187=DIRECTION('center_axis',(0.,1.,0.));
#10188=DIRECTION('ref_axis',(1.,0.,0.));
#10189=DIRECTION('',(0.,1.,0.));
#10190=DIRECTION('center_axis',(0.,-1.,0.));
#10191=DIRECTION('ref_axis',(1.,0.,0.));
#10192=DIRECTION('center_axis',(0.,1.,0.));
#10193=DIRECTION('ref_axis',(1.,0.,0.));
#10194=DIRECTION('center_axis',(0.,-1.,0.));
#10195=DIRECTION('ref_axis',(1.,0.,0.));
#10196=DIRECTION('',(0.,-1.,0.));
#10197=DIRECTION('center_axis',(0.,-1.,0.));
#10198=DIRECTION('ref_axis',(1.,0.,0.));
#10199=DIRECTION('center_axis',(0.,1.,0.));
#10200=DIRECTION('ref_axis',(1.,0.,0.));
#10201=DIRECTION('center_axis',(0.,1.,0.));
#10202=DIRECTION('ref_axis',(1.,0.,0.));
#10203=DIRECTION('',(0.,-1.,0.));
#10204=DIRECTION('center_axis',(0.,1.,0.));
#10205=DIRECTION('ref_axis',(1.,0.,0.));
#10206=DIRECTION('center_axis',(0.,1.,0.));
#10207=DIRECTION('ref_axis',(1.,0.,0.));
#10208=DIRECTION('center_axis',(0.,1.,0.));
#10209=DIRECTION('ref_axis',(1.,0.,0.));
#13065=CARTESIAN_POINT('',(0.,0.,0.));
#13066=CARTESIAN_POINT('Origin',(-1.23743686707646,-1.5,12.7625631329235));
#13067=CARTESIAN_POINT('',(-1.46243686707646,-1.4,12.7625631329235));
#13068=CARTESIAN_POINT('Origin',(-1.23743686707646,-1.4,12.7625631329235));
#13069=CARTESIAN_POINT('',(-1.46243686707646,-1.05,12.7625631329235));
#13070=CARTESIAN_POINT('',(-1.46243686707646,-1.5,12.7625631329235));
#13071=CARTESIAN_POINT('Origin',(-1.23743686707646,-1.05,12.7625631329235));
#13072=CARTESIAN_POINT('Origin',(-1.23743686707646,-1.5,15.2374368670765));
#13073=CARTESIAN_POINT('',(-1.46243686707646,-1.4,15.2374368670765));
#13074=CARTESIAN_POINT('Origin',(-1.23743686707646,-1.4,15.2374368670765));
#13075=CARTESIAN_POINT('',(-1.46243686707646,-1.05,15.2374368670765));
#13076=CARTESIAN_POINT('',(-1.46243686707646,-1.5,15.2374368670765));
#13077=CARTESIAN_POINT('Origin',(-1.23743686707646,-1.05,15.2374368670765));
#13078=CARTESIAN_POINT('Origin',(1.23743686707646,-1.5,15.2374368670765));
#13079=CARTESIAN_POINT('',(1.01243686707646,-1.4,15.2374368670765));
#13080=CARTESIAN_POINT('Origin',(1.23743686707646,-1.4,15.2374368670765));
#13081=CARTESIAN_POINT('',(1.01243686707646,-1.05,15.2374368670765));
#13082=CARTESIAN_POINT('',(1.01243686707646,-1.5,15.2374368670765));
#13083=CARTESIAN_POINT('Origin',(1.23743686707646,-1.05,15.2374368670765));
#13084=CARTESIAN_POINT('Origin',(1.23743686707646,-1.5,12.7625631329235));
#13085=CARTESIAN_POINT('',(1.01243686707646,-1.4,12.7625631329235));
#13086=CARTESIAN_POINT('Origin',(1.23743686707646,-1.4,12.7625631329235));
#13087=CARTESIAN_POINT('',(1.01243686707646,-1.05,12.7625631329235));
#13088=CARTESIAN_POINT('',(1.01243686707646,-1.5,12.7625631329235));
#13089=CARTESIAN_POINT('Origin',(1.23743686707646,-1.05,12.7625631329235));
#13090=CARTESIAN_POINT('Origin',(0.,-1.4,14.));
#13091=CARTESIAN_POINT('',(-1.02,-1.05,14.));
#13092=CARTESIAN_POINT('Origin',(0.,-1.05,14.));
#13093=CARTESIAN_POINT('',(-1.02,-1.4,14.));
#13094=CARTESIAN_POINT('',(-1.02,-1.4,14.));
#13095=CARTESIAN_POINT('Origin',(0.,-1.4,14.));
#13096=CARTESIAN_POINT('Origin',(0.,-1.4,14.));
#13097=CARTESIAN_POINT('',(-2.2,-1.05,14.));
#13098=CARTESIAN_POINT('Origin',(0.,-1.05,14.));
#13099=CARTESIAN_POINT('',(-2.2,-1.4,14.));
#13100=CARTESIAN_POINT('',(-2.2,-1.4,14.));
#13101=CARTESIAN_POINT('Origin',(0.,-1.4,14.));
#13102=CARTESIAN_POINT('Origin',(0.,-1.05,14.));
#13103=CARTESIAN_POINT('Origin',(0.,-1.4,14.));
#14430=UNCERTAINTY_MEASURE_WITH_UNIT(LENGTH_MEASURE(0.001),#14513,
'DISTANCE_ACCURACY_VALUE',
'Maximum model space distance between geometric entities at asserted c
onnectivities');
#14455=UNCERTAINTY_MEASURE_WITH_UNIT(LENGTH_MEASURE(0.001),#14513,
'DISTANCE_ACCURACY_VALUE',
'Maximum model space distance between geometric entities at asserted c
onnectivities');
#14487=(
GEOMETRIC_REPRESENTATION_CONTEXT(3)
GLOBAL_UNCERTAINTY_ASSIGNED_CONTEXT((#14430))
GLOBAL_UNIT_ASSIGNED_CONTEXT((#14513,#14515,#14516))
REPRESENTATION_CONTEXT('','3D')
);
#14512=(
GEOMETRIC_REPRESENTATION_CONTEXT(3)
GLOBAL_UNCERTAINTY_ASSIGNED_CONTEXT((#14455))
GLOBAL_UNIT_ASSIGNED_CONTEXT((#14513,#14515,#14516))
REPRESENTATION_CONTEXT('','3D')
);
#14513=(
LENGTH_UNIT()
NAMED_UNIT(*)
SI_UNIT(.CENTI.,.METRE.)
);
#14515=(
NAMED_UNIT(*)
PLANE_ANGLE_UNIT()
SI_UNIT($,.RADIAN.)
);
#14516=(
NAMED_UNIT(*)
SI_UNIT($,.STERADIAN.)
SOLID_ANGLE_UNIT()
);
#14548=SHAPE_DEFINITION_REPRESENTATION(#14604,#14772);
#14604=PRODUCT_DEFINITION_SHAPE('',$,#14829);
#14772=SHAPE_REPRESENTATION('',(#8413),#14487);
#14797=PRODUCT_DEFINITION_CONTEXT('part definition',#14967,'design');
#14829=PRODUCT_DEFINITION('Bearing cap (4)','Bearing cap (4)',#14885,#14797);
#14885=PRODUCT_DEFINITION_FORMATION('',$,#15000);
#14967=APPLICATION_CONTEXT(
'Core Data for Automotive Mechanical Design Process');
#14968=PRODUCT_CONTEXT('part definition',#14967,'mechanical');
#15000=PRODUCT('Bearing cap (4)','Bearing cap (4)','Bearing cap (4)',(#14968));
#15081=COLOUR_RGB('Grey',0.48,0.52,0.57);
#15082=FILL_AREA_STYLE_COLOUR('',#15081);
#15083=FILL_AREA_STYLE('',(#15082));
#15084=SURFACE_STYLE_FILL_AREA(#15083);
#15085=SURFACE_SIDE_STYLE('',(#15084));
#15086=SURFACE_STYLE_USAGE(.BOTH.,#15085);
#15087=PRESENTATION_STYLE_ASSIGNMENT((#15086));
ENDSEC;
END-ISO-10303-21;
